ISO-10303-21;
HEADER;
/* Generated by software containing ST-Developer
 * from STEP Tools, Inc. (www.steptools.com) 
 */

FILE_DESCRIPTION(
/* description */ ('Belt tension measurement rig'),
/* implementation_level */ '2;1');

FILE_NAME(
/* name */ 'Screw support.step',
/* time_stamp */ '2026-10-28T03:24:44-07:00',
/* author */ (''),
/* organization */ (''),
/* preprocessor_version */ 'ST-DEVELOPER v20.2',
/* originating_system */ 'Autodesk Translation Framework v15.17.0.0',
/* authorisation */ '');

FILE_SCHEMA (('AUTOMOTIVE_DESIGN { 1 0 10303 214 3 1 1 }'));
ENDSEC;

DATA;
#10=MECHANICAL_DESIGN_GEOMETRIC_PRESENTATION_REPRESENTATION('',(#699),#23587);
#589=SHAPE_REPRESENTATION_RELATIONSHIP('SRR','None',#23834,#644);
#644=ADVANCED_BREP_SHAPE_REPRESENTATION('',(#769),#23532);
#699=STYLED_ITEM('',(#24218),#769);
#769=MANIFOLD_SOLID_BREP('Body1',#12204);
#869=FACE_BOUND('',#2193,.T.);
#870=FACE_BOUND('',#2196,.T.);
#871=FACE_BOUND('',#2202,.T.);
#872=FACE_BOUND('',#2205,.T.);
#873=FACE_BOUND('',#2207,.T.);
#874=FACE_BOUND('',#2208,.T.);
#875=FACE_BOUND('',#2210,.T.);
#876=FACE_BOUND('',#2211,.T.);
#1087=PLANE('',#13074);
#1088=PLANE('',#13079);
#1089=PLANE('',#13088);
#1090=PLANE('',#13089);
#1091=PLANE('',#13090);
#1092=PLANE('',#13091);
#1093=PLANE('',#13092);
#1094=PLANE('',#13093);
#1447=FACE_OUTER_BOUND('',#2191,.T.);
#1448=FACE_OUTER_BOUND('',#2192,.T.);
#1449=FACE_OUTER_BOUND('',#2194,.T.);
#1450=FACE_OUTER_BOUND('',#2195,.T.);
#1451=FACE_OUTER_BOUND('',#2197,.T.);
#1452=FACE_OUTER_BOUND('',#2198,.T.);
#1453=FACE_OUTER_BOUND('',#2199,.T.);
#1454=FACE_OUTER_BOUND('',#2200,.T.);
#1455=FACE_OUTER_BOUND('',#2201,.T.);
#1456=FACE_OUTER_BOUND('',#2203,.T.);
#1457=FACE_OUTER_BOUND('',#2204,.T.);
#1458=FACE_OUTER_BOUND('',#2206,.T.);
#1459=FACE_OUTER_BOUND('',#2209,.T.);
#2191=EDGE_LOOP('',(#8328,#8329,#8330,#8331));
#2192=EDGE_LOOP('',(#8332));
#2193=EDGE_LOOP('',(#8333));
#2194=EDGE_LOOP('',(#8334,#8335,#8336,#8337));
#2195=EDGE_LOOP('',(#8338));
#2196=EDGE_LOOP('',(#8339));
#2197=EDGE_LOOP('',(#8340,#8341,#8342,#8343));
#2198=EDGE_LOOP('',(#8344,#8345,#8346,#8347));
#2199=EDGE_LOOP('',(#8348,#8349,#8350,#8351));
#2200=EDGE_LOOP('',(#8352,#8353,#8354,#8355));
#2201=EDGE_LOOP('',(#8356,#8357,#8358,#8359));
#2202=EDGE_LOOP('',(#8360));
#2203=EDGE_LOOP('',(#8361,#8362,#8363,#8364));
#2204=EDGE_LOOP('',(#8365,#8366,#8367,#8368));
#2205=EDGE_LOOP('',(#8369));
#2206=EDGE_LOOP('',(#8370,#8371,#8372,#8373));
#2207=EDGE_LOOP('',(#8374));
#2208=EDGE_LOOP('',(#8375));
#2209=EDGE_LOOP('',(#8376,#8377,#8378,#8379));
#2210=EDGE_LOOP('',(#8380));
#2211=EDGE_LOOP('',(#8381));
#3073=LINE('',#18984,#3824);
#3074=LINE('',#18993,#3825);
#3075=LINE('',#19001,#3826);
#3076=LINE('',#19005,#3827);
#3077=LINE('',#19010,#3828);
#3078=LINE('',#19015,#3829);
#3079=LINE('',#19017,#3830);
#3080=LINE('',#19019,#3831);
#3081=LINE('',#19020,#3832);
#3082=LINE('',#19023,#3833);
#3083=LINE('',#19025,#3834);
#3084=LINE('',#19026,#3835);
#3085=LINE('',#19029,#3836);
#3086=LINE('',#19031,#3837);
#3087=LINE('',#19032,#3838);
#3088=LINE('',#19034,#3839);
#3089=LINE('',#19035,#3840);
#3824=VECTOR('',#15016,0.4);
#3825=VECTOR('',#15027,0.4);
#3826=VECTOR('',#15038,0.225);
#3827=VECTOR('',#15043,0.225);
#3828=VECTOR('',#15048,0.8);
#3829=VECTOR('',#15053,1.);
#3830=VECTOR('',#15054,1.);
#3831=VECTOR('',#15055,1.);
#3832=VECTOR('',#15056,1.);
#3833=VECTOR('',#15059,1.);
#3834=VECTOR('',#15060,1.);
#3835=VECTOR('',#15061,1.);
#3836=VECTOR('',#15064,1.);
#3837=VECTOR('',#15065,1.);
#3838=VECTOR('',#15066,1.);
#3839=VECTOR('',#15069,1.);
#3840=VECTOR('',#15070,1.);
#4560=CIRCLE('',#13072,0.4);
#4561=CIRCLE('',#13073,0.4);
#4562=CIRCLE('',#13075,0.225);
#4563=CIRCLE('',#13077,0.4);
#4564=CIRCLE('',#13078,0.4);
#4565=CIRCLE('',#13080,0.225);
#4566=CIRCLE('',#13082,0.225);
#4567=CIRCLE('',#13084,0.225);
#4568=CIRCLE('',#13086,0.8);
#4569=CIRCLE('',#13087,0.8);
#5368=VERTEX_POINT('',#18981);
#5369=VERTEX_POINT('',#18983);
#5370=VERTEX_POINT('',#18987);
#5371=VERTEX_POINT('',#18990);
#5372=VERTEX_POINT('',#18992);
#5373=VERTEX_POINT('',#18996);
#5374=VERTEX_POINT('',#18999);
#5375=VERTEX_POINT('',#19003);
#5376=VERTEX_POINT('',#19007);
#5377=VERTEX_POINT('',#19009);
#5378=VERTEX_POINT('',#19013);
#5379=VERTEX_POINT('',#19014);
#5380=VERTEX_POINT('',#19016);
#5381=VERTEX_POINT('',#19018);
#5382=VERTEX_POINT('',#19022);
#5383=VERTEX_POINT('',#19024);
#5384=VERTEX_POINT('',#19028);
#5385=VERTEX_POINT('',#19030);
#6523=EDGE_CURVE('',#5368,#5368,#4560,.T.);
#6524=EDGE_CURVE('',#5368,#5369,#3073,.T.);
#6525=EDGE_CURVE('',#5369,#5369,#4561,.T.);
#6526=EDGE_CURVE('',#5370,#5370,#4562,.T.);
#6527=EDGE_CURVE('',#5371,#5371,#4563,.T.);
#6528=EDGE_CURVE('',#5371,#5372,#3074,.T.);
#6529=EDGE_CURVE('',#5372,#5372,#4564,.T.);
#6530=EDGE_CURVE('',#5373,#5373,#4565,.T.);
#6531=EDGE_CURVE('',#5374,#5374,#4566,.T.);
#6532=EDGE_CURVE('',#5374,#5370,#3075,.T.);
#6533=EDGE_CURVE('',#5375,#5375,#4567,.T.);
#6534=EDGE_CURVE('',#5375,#5373,#3076,.T.);
#6535=EDGE_CURVE('',#5376,#5376,#4568,.T.);
#6536=EDGE_CURVE('',#5376,#5377,#3077,.T.);
#6537=EDGE_CURVE('',#5377,#5377,#4569,.T.);
#6538=EDGE_CURVE('',#5378,#5379,#3078,.T.);
#6539=EDGE_CURVE('',#5379,#5380,#3079,.T.);
#6540=EDGE_CURVE('',#5381,#5380,#3080,.T.);
#6541=EDGE_CURVE('',#5378,#5381,#3081,.T.);
#6542=EDGE_CURVE('',#5382,#5378,#3082,.T.);
#6543=EDGE_CURVE('',#5383,#5381,#3083,.T.);
#6544=EDGE_CURVE('',#5382,#5383,#3084,.T.);
#6545=EDGE_CURVE('',#5384,#5382,#3085,.T.);
#6546=EDGE_CURVE('',#5385,#5383,#3086,.T.);
#6547=EDGE_CURVE('',#5384,#5385,#3087,.T.);
#6548=EDGE_CURVE('',#5379,#5384,#3088,.T.);
#6549=EDGE_CURVE('',#5380,#5385,#3089,.T.);
#8328=ORIENTED_EDGE('',*,*,#6523,.F.);
#8329=ORIENTED_EDGE('',*,*,#6524,.T.);
#8330=ORIENTED_EDGE('',*,*,#6525,.F.);
#8331=ORIENTED_EDGE('',*,*,#6524,.F.);
#8332=ORIENTED_EDGE('',*,*,#6523,.T.);
#8333=ORIENTED_EDGE('',*,*,#6526,.F.);
#8334=ORIENTED_EDGE('',*,*,#6527,.F.);
#8335=ORIENTED_EDGE('',*,*,#6528,.T.);
#8336=ORIENTED_EDGE('',*,*,#6529,.F.);
#8337=ORIENTED_EDGE('',*,*,#6528,.F.);
#8338=ORIENTED_EDGE('',*,*,#6527,.T.);
#8339=ORIENTED_EDGE('',*,*,#6530,.F.);
#8340=ORIENTED_EDGE('',*,*,#6531,.F.);
#8341=ORIENTED_EDGE('',*,*,#6532,.T.);
#8342=ORIENTED_EDGE('',*,*,#6526,.T.);
#8343=ORIENTED_EDGE('',*,*,#6532,.F.);
#8344=ORIENTED_EDGE('',*,*,#6533,.F.);
#8345=ORIENTED_EDGE('',*,*,#6534,.T.);
#8346=ORIENTED_EDGE('',*,*,#6530,.T.);
#8347=ORIENTED_EDGE('',*,*,#6534,.F.);
#8348=ORIENTED_EDGE('',*,*,#6535,.F.);
#8349=ORIENTED_EDGE('',*,*,#6536,.T.);
#8350=ORIENTED_EDGE('',*,*,#6537,.F.);
#8351=ORIENTED_EDGE('',*,*,#6536,.F.);
#8352=ORIENTED_EDGE('',*,*,#6538,.T.);
#8353=ORIENTED_EDGE('',*,*,#6539,.T.);
#8354=ORIENTED_EDGE('',*,*,#6540,.F.);
#8355=ORIENTED_EDGE('',*,*,#6541,.F.);
#8356=ORIENTED_EDGE('',*,*,#6542,.T.);
#8357=ORIENTED_EDGE('',*,*,#6541,.T.);
#8358=ORIENTED_EDGE('',*,*,#6543,.F.);
#8359=ORIENTED_EDGE('',*,*,#6544,.F.);
#8360=ORIENTED_EDGE('',*,*,#6537,.T.);
#8361=ORIENTED_EDGE('',*,*,#6545,.T.);
#8362=ORIENTED_EDGE('',*,*,#6544,.T.);
#8363=ORIENTED_EDGE('',*,*,#6546,.F.);
#8364=ORIENTED_EDGE('',*,*,#6547,.F.);
#8365=ORIENTED_EDGE('',*,*,#6548,.T.);
#8366=ORIENTED_EDGE('',*,*,#6547,.T.);
#8367=ORIENTED_EDGE('',*,*,#6549,.F.);
#8368=ORIENTED_EDGE('',*,*,#6539,.F.);
#8369=ORIENTED_EDGE('',*,*,#6535,.T.);
#8370=ORIENTED_EDGE('',*,*,#6549,.T.);
#8371=ORIENTED_EDGE('',*,*,#6546,.T.);
#8372=ORIENTED_EDGE('',*,*,#6543,.T.);
#8373=ORIENTED_EDGE('',*,*,#6540,.T.);
#8374=ORIENTED_EDGE('',*,*,#6525,.T.);
#8375=ORIENTED_EDGE('',*,*,#6529,.T.);
#8376=ORIENTED_EDGE('',*,*,#6548,.F.);
#8377=ORIENTED_EDGE('',*,*,#6538,.F.);
#8378=ORIENTED_EDGE('',*,*,#6542,.F.);
#8379=ORIENTED_EDGE('',*,*,#6545,.F.);
#8380=ORIENTED_EDGE('',*,*,#6531,.T.);
#8381=ORIENTED_EDGE('',*,*,#6533,.T.);
#11203=CYLINDRICAL_SURFACE('',#13071,0.4);
#11204=CYLINDRICAL_SURFACE('',#13076,0.4);
#11205=CYLINDRICAL_SURFACE('',#13081,0.225);
#11206=CYLINDRICAL_SURFACE('',#13083,0.225);
#11207=CYLINDRICAL_SURFACE('',#13085,0.8);
#11588=ADVANCED_FACE('',(#1447),#11203,.F.);
#11589=ADVANCED_FACE('',(#1448,#869),#1087,.T.);
#11590=ADVANCED_FACE('',(#1449),#11204,.F.);
#11591=ADVANCED_FACE('',(#1450,#870),#1088,.T.);
#11592=ADVANCED_FACE('',(#1451),#11205,.F.);
#11593=ADVANCED_FACE('',(#1452),#11206,.F.);
#11594=ADVANCED_FACE('',(#1453),#11207,.F.);
#11595=ADVANCED_FACE('',(#1454),#1089,.T.);
#11596=ADVANCED_FACE('',(#1455,#871),#1090,.T.);
#11597=ADVANCED_FACE('',(#1456),#1091,.T.);
#11598=ADVANCED_FACE('',(#1457,#872),#1092,.T.);
#11599=ADVANCED_FACE('',(#1458,#873,#874),#1093,.T.);
#11600=ADVANCED_FACE('',(#1459,#875,#876),#1094,.F.);
#12204=CLOSED_SHELL('',(#11588,#11589,#11590,#11591,#11592,#11593,#11594,
#11595,#11596,#11597,#11598,#11599,#11600));
#13070=AXIS2_PLACEMENT_3D('',#18979,#15010,#15011);
#13071=AXIS2_PLACEMENT_3D('',#18980,#15012,#15013);
#13072=AXIS2_PLACEMENT_3D('',#18982,#15014,#15015);
#13073=AXIS2_PLACEMENT_3D('',#18985,#15017,#15018);
#13074=AXIS2_PLACEMENT_3D('',#18986,#15019,#15020);
#13075=AXIS2_PLACEMENT_3D('',#18988,#15021,#15022);
#13076=AXIS2_PLACEMENT_3D('',#18989,#15023,#15024);
#13077=AXIS2_PLACEMENT_3D('',#18991,#15025,#15026);
#13078=AXIS2_PLACEMENT_3D('',#18994,#15028,#15029);
#13079=AXIS2_PLACEMENT_3D('',#18995,#15030,#15031);
#13080=AXIS2_PLACEMENT_3D('',#18997,#15032,#15033);
#13081=AXIS2_PLACEMENT_3D('',#18998,#15034,#15035);
#13082=AXIS2_PLACEMENT_3D('',#19000,#15036,#15037);
#13083=AXIS2_PLACEMENT_3D('',#19002,#15039,#15040);
#13084=AXIS2_PLACEMENT_3D('',#19004,#15041,#15042);
#13085=AXIS2_PLACEMENT_3D('',#19006,#15044,#15045);
#13086=AXIS2_PLACEMENT_3D('',#19008,#15046,#15047);
#13087=AXIS2_PLACEMENT_3D('',#19011,#15049,#15050);
#13088=AXIS2_PLACEMENT_3D('',#19012,#15051,#15052);
#13089=AXIS2_PLACEMENT_3D('',#19021,#15057,#15058);
#13090=AXIS2_PLACEMENT_3D('',#19027,#15062,#15063);
#13091=AXIS2_PLACEMENT_3D('',#19033,#15067,#15068);
#13092=AXIS2_PLACEMENT_3D('',#19036,#15071,#15072);
#13093=AXIS2_PLACEMENT_3D('',#19037,#15073,#15074);
#15010=DIRECTION('axis',(0.,0.,1.));
#15011=DIRECTION('refdir',(1.,0.,0.));
#15012=DIRECTION('center_axis',(0.,0.,1.));
#15013=DIRECTION('ref_axis',(1.,0.,0.));
#15014=DIRECTION('center_axis',(0.,0.,1.));
#15015=DIRECTION('ref_axis',(1.,0.,0.));
#15016=DIRECTION('',(0.,0.,1.));
#15017=DIRECTION('center_axis',(0.,0.,-1.));
#15018=DIRECTION('ref_axis',(1.,0.,0.));
#15019=DIRECTION('center_axis',(0.,0.,1.));
#15020=DIRECTION('ref_axis',(1.,0.,0.));
#15021=DIRECTION('center_axis',(0.,0.,1.));
#15022=DIRECTION('ref_axis',(1.,0.,0.));
#15023=DIRECTION('center_axis',(0.,0.,1.));
#15024=DIRECTION('ref_axis',(1.,0.,0.));
#15025=DIRECTION('center_axis',(0.,0.,1.));
#15026=DIRECTION('ref_axis',(1.,0.,0.));
#15027=DIRECTION('',(0.,0.,1.));
#15028=DIRECTION('center_axis',(0.,0.,-1.));
#15029=DIRECTION('ref_axis',(1.,0.,0.));
#15030=DIRECTION('center_axis',(0.,0.,1.));
#15031=DIRECTION('ref_axis',(1.,0.,0.));
#15032=DIRECTION('center_axis',(0.,0.,1.));
#15033=DIRECTION('ref_axis',(1.,0.,0.));
#15034=DIRECTION('center_axis',(0.,0.,1.));
#15035=DIRECTION('ref_axis',(1.,0.,0.));
#15036=DIRECTION('center_axis',(0.,0.,1.));
#15037=DIRECTION('ref_axis',(1.,0.,0.));
#15038=DIRECTION('',(0.,0.,1.));
#15039=DIRECTION('center_axis',(0.,0.,1.));
#15040=DIRECTION('ref_axis',(1.,0.,0.));
#15041=DIRECTION('center_axis',(0.,0.,1.));
#15042=DIRECTION('ref_axis',(1.,0.,0.));
#15043=DIRECTION('',(0.,0.,1.));
#15044=DIRECTION('center_axis',(1.,0.,0.));
#15045=DIRECTION('ref_axis',(0.,0.,-1.));
#15046=DIRECTION('center_axis',(1.,0.,0.));
#15047=DIRECTION('ref_axis',(0.,0.,-1.));
#15048=DIRECTION('',(1.,0.,0.));
#15049=DIRECTION('center_axis',(-1.,0.,0.));
#15050=DIRECTION('ref_axis',(0.,0.,-1.));
#15051=DIRECTION('center_axis',(0.,1.,0.));
#15052=DIRECTION('ref_axis',(-1.,0.,0.));
#15053=DIRECTION('',(-1.,0.,0.));
#15054=DIRECTION('',(0.,0.,1.));
#15055=DIRECTION('',(-1.,0.,0.));
#15056=DIRECTION('',(0.,0.,1.));
#15057=DIRECTION('center_axis',(1.,0.,0.));
#15058=DIRECTION('ref_axis',(0.,1.,0.));
#15059=DIRECTION('',(0.,1.,0.));
#15060=DIRECTION('',(0.,1.,0.));
#15061=DIRECTION('',(0.,0.,1.));
#15062=DIRECTION('center_axis',(0.,-1.,0.));
#15063=DIRECTION('ref_axis',(1.,0.,0.));
#15064=DIRECTION('',(1.,0.,0.));
#15065=DIRECTION('',(1.,0.,0.));
#15066=DIRECTION('',(0.,0.,1.));
#15067=DIRECTION('center_axis',(-1.,0.,0.));
#15068=DIRECTION('ref_axis',(0.,-1.,0.));
#15069=DIRECTION('',(0.,-1.,0.));
#15070=DIRECTION('',(0.,-1.,0.));
#15071=DIRECTION('center_axis',(0.,0.,1.));
#15072=DIRECTION('ref_axis',(1.,0.,0.));
#15073=DIRECTION('center_axis',(0.,0.,1.));
#15074=DIRECTION('ref_axis',(1.,0.,0.));
#18979=CARTESIAN_POINT('',(0.,0.,0.));
#18980=CARTESIAN_POINT('Origin',(2.75,9.5,0.6));
#18981=CARTESIAN_POINT('',(2.35,9.5,0.6));
#18982=CARTESIAN_POINT('Origin',(2.75,9.5,0.6));
#18983=CARTESIAN_POINT('',(2.35,9.5,6.));
#18984=CARTESIAN_POINT('',(2.35,9.5,0.6));
#18985=CARTESIAN_POINT('Origin',(2.75,9.5,6.));
#18986=CARTESIAN_POINT('Origin',(2.75,9.5,0.6));
#18987=CARTESIAN_POINT('',(2.525,9.5,0.6));
#18988=CARTESIAN_POINT('Origin',(2.75,9.5,0.6));
#18989=CARTESIAN_POINT('Origin',(2.75,12.5,0.6));
#18990=CARTESIAN_POINT('',(2.35,12.5,0.6));
#18991=CARTESIAN_POINT('Origin',(2.75,12.5,0.6));
#18992=CARTESIAN_POINT('',(2.35,12.5,6.));
#18993=CARTESIAN_POINT('',(2.35,12.5,0.6));
#18994=CARTESIAN_POINT('Origin',(2.75,12.5,6.));
#18995=CARTESIAN_POINT('Origin',(2.75,12.5,0.6));
#18996=CARTESIAN_POINT('',(2.525,12.5,0.6));
#18997=CARTESIAN_POINT('Origin',(2.75,12.5,0.6));
#18998=CARTESIAN_POINT('Origin',(2.75,9.5,-0.1));
#18999=CARTESIAN_POINT('',(2.525,9.5,0.));
#19000=CARTESIAN_POINT('Origin',(2.75,9.5,0.));
#19001=CARTESIAN_POINT('',(2.525,9.5,-0.1));
#19002=CARTESIAN_POINT('Origin',(2.75,12.5,-0.1));
#19003=CARTESIAN_POINT('',(2.525,12.5,0.));
#19004=CARTESIAN_POINT('Origin',(2.75,12.5,0.));
#19005=CARTESIAN_POINT('',(2.525,12.5,-0.1));
#19006=CARTESIAN_POINT('Origin',(1.9,11.,4.5));
#19007=CARTESIAN_POINT('',(2.,11.,5.3));
#19008=CARTESIAN_POINT('Origin',(2.,11.,4.5));
#19009=CARTESIAN_POINT('',(3.5,11.,5.3));
#19010=CARTESIAN_POINT('',(1.9,11.,5.3));
#19011=CARTESIAN_POINT('Origin',(3.5,11.,4.5));
#19012=CARTESIAN_POINT('Origin',(3.5,13.,0.));
#19013=CARTESIAN_POINT('',(3.5,13.,0.));
#19014=CARTESIAN_POINT('',(2.,13.,0.));
#19015=CARTESIAN_POINT('',(3.5,13.,0.));
#19016=CARTESIAN_POINT('',(2.,13.,6.));
#19017=CARTESIAN_POINT('',(2.,13.,0.));
#19018=CARTESIAN_POINT('',(3.5,13.,6.));
#19019=CARTESIAN_POINT('',(3.5,13.,6.));
#19020=CARTESIAN_POINT('',(3.5,13.,0.));
#19021=CARTESIAN_POINT('Origin',(3.5,9.,0.));
#19022=CARTESIAN_POINT('',(3.5,9.,0.));
#19023=CARTESIAN_POINT('',(3.5,9.,0.));
#19024=CARTESIAN_POINT('',(3.5,9.,6.));
#19025=CARTESIAN_POINT('',(3.5,9.,6.));
#19026=CARTESIAN_POINT('',(3.5,9.,0.));
#19027=CARTESIAN_POINT('Origin',(2.,9.,0.));
#19028=CARTESIAN_POINT('',(2.,9.,0.));
#19029=CARTESIAN_POINT('',(2.,9.,0.));
#19030=CARTESIAN_POINT('',(2.,9.,6.));
#19031=CARTESIAN_POINT('',(2.,9.,6.));
#19032=CARTESIAN_POINT('',(2.,9.,0.));
#19033=CARTESIAN_POINT('Origin',(2.,13.,0.));
#19034=CARTESIAN_POINT('',(2.,13.,0.));
#19035=CARTESIAN_POINT('',(2.,13.,6.));
#19036=CARTESIAN_POINT('Origin',(2.75,11.,6.));
#19037=CARTESIAN_POINT('Origin',(2.75,11.,0.));
#23467=UNCERTAINTY_MEASURE_WITH_UNIT(LENGTH_MEASURE(0.001),#23588,
'DISTANCE_ACCURACY_VALUE',
'Maximum model space distance between geometric entities at asserted c
onnectivities');
#23522=UNCERTAINTY_MEASURE_WITH_UNIT(LENGTH_MEASURE(0.001),#23588,
'DISTANCE_ACCURACY_VALUE',
'Maximum model space distance between geometric entities at asserted c
onnectivities');
#23532=(
GEOMETRIC_REPRESENTATION_CONTEXT(3)
GLOBAL_UNCERTAINTY_ASSIGNED_CONTEXT((#23467))
GLOBAL_UNIT_ASSIGNED_CONTEXT((#23588,#23590,#23591))
REPRESENTATION_CONTEXT('','3D')
);
#23587=(
GEOMETRIC_REPRESENTATION_CONTEXT(3)
GLOBAL_UNCERTAINTY_ASSIGNED_CONTEXT((#23522))
GLOBAL_UNIT_ASSIGNED_CONTEXT((#23588,#23590,#23591))
REPRESENTATION_CONTEXT('','3D')
);
#23588=(
LENGTH_UNIT()
NAMED_UNIT(*)
SI_UNIT(.CENTI.,.METRE.)
);
#23590=(
NAMED_UNIT(*)
PLANE_ANGLE_UNIT()
SI_UNIT($,.RADIAN.)
);
#23591=(
NAMED_UNIT(*)
SI_UNIT($,.STERADIAN.)
SOLID_ANGLE_UNIT()
);
#23601=SHAPE_DEFINITION_REPRESENTATION(#23665,#23834);
#23665=PRODUCT_DEFINITION_SHAPE('',$,#23899);
#23834=SHAPE_REPRESENTATION('',(#13070),#23532);
#23889=PRODUCT_DEFINITION_CONTEXT('part definition',#24083,'design');
#23899=PRODUCT_DEFINITION('Screw support','Screw support',#23963,#23889);
#23963=PRODUCT_DEFINITION_FORMATION('',$,#24094);
#24083=APPLICATION_CONTEXT(
'Core Data for Automotive Mechanical Design Process');
#24084=PRODUCT_CONTEXT('part definition',#24083,'mechanical');
#24094=PRODUCT('Screw support','Screw support','Screw support',(#24084));
#24212=COLOUR_RGB('Black',0.12,0.14,0.17);
#24213=FILL_AREA_STYLE_COLOUR('',#24212);
#24214=FILL_AREA_STYLE('',(#24213));
#24215=SURFACE_STYLE_FILL_AREA(#24214);
#24216=SURFACE_SIDE_STYLE('',(#24215));
#24217=SURFACE_STYLE_USAGE(.BOTH.,#24216);
#24218=PRESENTATION_STYLE_ASSIGNMENT((#24217));
ENDSEC;
END-ISO-10303-21;
